ISO-10303-21;
HEADER;
/* Generated by software containing ST-Developer
 * from STEP Tools, Inc. (www.steptools.com) 
 */

FILE_DESCRIPTION(
/* description */ ('Union bypass pipe loop'),
/* implementation_level */ '2;1');

FILE_NAME(
/* name */ 'Cap Screw - M4x16.step',
/* time_stamp */ '2026-10-27T21:00:29-07:00',
/* author */ (''),
/* organization */ (''),
/* preprocessor_version */ 'ST-DEVELOPER v20.2',
/* originating_system */ 'Autodesk Translation Framework v15.17.0.0',
/* authorisation */ '');

FILE_SCHEMA (('AUTOMOTIVE_DESIGN { 1 0 10303 214 3 1 1 }'));
ENDSEC;

DATA;
#10=MECHANICAL_DESIGN_GEOMETRIC_PRESENTATION_REPRESENTATION('',(#457),#10095);
#357=CONICAL_SURFACE('',#6159,0.325,0.785398163397448);
#358=CONICAL_SURFACE('',#6163,0.335,0.785398163397448);
#359=CONICAL_SURFACE('',#6167,0.21,0.463647609000806);
#360=CONICAL_SURFACE('',#6171,0.18,0.785398163397448);
#373=ORIENTED_CLOSED_SHELL('',*,#5530,.F.);
#377=BREP_WITH_VOIDS('Body1',#5529,(#373));
#393=SHAPE_REPRESENTATION_RELATIONSHIP('SRR','None',#10262,#425);
#425=ADVANCED_BREP_SHAPE_REPRESENTATION('',(#377),#10074);
#457=STYLED_ITEM('',(#10507),#377);
#576=FACE_BOUND('',#1366,.T.);
#708=PLANE('',#6157);
#709=PLANE('',#6165);
#710=PLANE('',#6173);
#711=PLANE('',#6174);
#712=PLANE('',#6175);
#713=PLANE('',#6176);
#714=PLANE('',#6177);
#715=PLANE('',#6178);
#716=PLANE('',#6179);
#717=PLANE('',#6180);
#718=PLANE('',#6181);
#964=FACE_OUTER_BOUND('',#1361,.T.);
#965=FACE_OUTER_BOUND('',#1362,.T.);
#966=FACE_OUTER_BOUND('',#1363,.T.);
#967=FACE_OUTER_BOUND('',#1364,.T.);
#968=FACE_OUTER_BOUND('',#1365,.T.);
#969=FACE_OUTER_BOUND('',#1367,.T.);
#970=FACE_OUTER_BOUND('',#1368,.T.);
#971=FACE_OUTER_BOUND('',#1369,.T.);
#972=FACE_OUTER_BOUND('',#1370,.T.);
#973=FACE_OUTER_BOUND('',#1371,.T.);
#974=FACE_OUTER_BOUND('',#1372,.T.);
#975=FACE_OUTER_BOUND('',#1373,.T.);
#976=FACE_OUTER_BOUND('',#1374,.T.);
#977=FACE_OUTER_BOUND('',#1375,.T.);
#978=FACE_OUTER_BOUND('',#1376,.T.);
#979=FACE_OUTER_BOUND('',#1377,.T.);
#980=FACE_OUTER_BOUND('',#1378,.T.);
#1361=EDGE_LOOP('',(#4270));
#1362=EDGE_LOOP('',(#4271,#4272,#4273,#4274));
#1363=EDGE_LOOP('',(#4275,#4276,#4277,#4278));
#1364=EDGE_LOOP('',(#4279,#4280,#4281,#4282));
#1365=EDGE_LOOP('',(#4283));
#1366=EDGE_LOOP('',(#4284));
#1367=EDGE_LOOP('',(#4285,#4286,#4287,#4288));
#1368=EDGE_LOOP('',(#4289,#4290,#4291,#4292));
#1369=EDGE_LOOP('',(#4293,#4294,#4295,#4296));
#1370=EDGE_LOOP('',(#4297));
#1371=EDGE_LOOP('',(#4298,#4299,#4300,#4301));
#1372=EDGE_LOOP('',(#4302,#4303,#4304,#4305));
#1373=EDGE_LOOP('',(#4306,#4307,#4308,#4309));
#1374=EDGE_LOOP('',(#4310,#4311,#4312,#4313));
#1375=EDGE_LOOP('',(#4314,#4315,#4316,#4317));
#1376=EDGE_LOOP('',(#4318,#4319,#4320,#4321));
#1377=EDGE_LOOP('',(#4322,#4323,#4324,#4325,#4326,#4327));
#1378=EDGE_LOOP('',(#4328,#4329,#4330,#4331,#4332,#4333));
#1770=LINE('',#9040,#2146);
#1771=LINE('',#9044,#2147);
#1772=LINE('',#9048,#2148);
#1773=LINE('',#9055,#2149);
#1774=LINE('',#9059,#2150);
#1775=LINE('',#9063,#2151);
#1776=LINE('',#9068,#2152);
#1777=LINE('',#9070,#2153);
#1778=LINE('',#9072,#2154);
#1779=LINE('',#9073,#2155);
#1780=LINE('',#9076,#2156);
#1781=LINE('',#9078,#2157);
#1782=LINE('',#9079,#2158);
#1783=LINE('',#9082,#2159);
#1784=LINE('',#9084,#2160);
#1785=LINE('',#9085,#2161);
#1786=LINE('',#9088,#2162);
#1787=LINE('',#9090,#2163);
#1788=LINE('',#9091,#2164);
#1789=LINE('',#9094,#2165);
#1790=LINE('',#9096,#2166);
#1791=LINE('',#9097,#2167);
#1792=LINE('',#9099,#2168);
#1793=LINE('',#9100,#2169);
#2146=VECTOR('',#7278,0.325);
#2147=VECTOR('',#7283,0.35);
#2148=VECTOR('',#7288,0.335);
#2149=VECTOR('',#7297,0.21);
#2150=VECTOR('',#7302,0.2);
#2151=VECTOR('',#7307,0.18);
#2152=VECTOR('',#7312,1.);
#2153=VECTOR('',#7313,1.);
#2154=VECTOR('',#7314,1.);
#2155=VECTOR('',#7315,1.);
#2156=VECTOR('',#7318,1.);
#2157=VECTOR('',#7319,1.);
#2158=VECTOR('',#7320,1.);
#2159=VECTOR('',#7323,1.);
#2160=VECTOR('',#7324,1.);
#2161=VECTOR('',#7325,1.);
#2162=VECTOR('',#7328,1.);
#2163=VECTOR('',#7329,1.);
#2164=VECTOR('',#7330,1.);
#2165=VECTOR('',#7333,1.);
#2166=VECTOR('',#7334,1.);
#2167=VECTOR('',#7335,1.);
#2168=VECTOR('',#7338,1.);
#2169=VECTOR('',#7339,1.);
#2482=CIRCLE('',#6158,0.3);
#2483=CIRCLE('',#6160,0.35);
#2484=CIRCLE('',#6162,0.35);
#2485=CIRCLE('',#6164,0.32);
#2486=CIRCLE('',#6166,0.22);
#2487=CIRCLE('',#6168,0.1954);
#2488=CIRCLE('',#6170,0.1954);
#2489=CIRCLE('',#6172,0.16);
#2806=VERTEX_POINT('',#9035);
#2807=VERTEX_POINT('',#9038);
#2808=VERTEX_POINT('',#9042);
#2809=VERTEX_POINT('',#9046);
#2810=VERTEX_POINT('',#9050);
#2811=VERTEX_POINT('',#9053);
#2812=VERTEX_POINT('',#9057);
#2813=VERTEX_POINT('',#9061);
#2814=VERTEX_POINT('',#9066);
#2815=VERTEX_POINT('',#9067);
#2816=VERTEX_POINT('',#9069);
#2817=VERTEX_POINT('',#9071);
#2818=VERTEX_POINT('',#9075);
#2819=VERTEX_POINT('',#9077);
#2820=VERTEX_POINT('',#9081);
#2821=VERTEX_POINT('',#9083);
#2822=VERTEX_POINT('',#9087);
#2823=VERTEX_POINT('',#9089);
#2824=VERTEX_POINT('',#9093);
#2825=VERTEX_POINT('',#9095);
#3333=EDGE_CURVE('',#2806,#2806,#2482,.T.);
#3334=EDGE_CURVE('',#2807,#2807,#2483,.T.);
#3335=EDGE_CURVE('',#2807,#2806,#1770,.T.);
#3336=EDGE_CURVE('',#2808,#2808,#2484,.T.);
#3337=EDGE_CURVE('',#2808,#2807,#1771,.T.);
#3338=EDGE_CURVE('',#2809,#2809,#2485,.T.);
#3339=EDGE_CURVE('',#2809,#2808,#1772,.T.);
#3340=EDGE_CURVE('',#2810,#2810,#2486,.T.);
#3341=EDGE_CURVE('',#2811,#2811,#2487,.F.);
#3342=EDGE_CURVE('',#2811,#2810,#1773,.T.);
#3343=EDGE_CURVE('',#2812,#2812,#2488,.F.);
#3344=EDGE_CURVE('',#2812,#2811,#1774,.T.);
#3345=EDGE_CURVE('',#2813,#2813,#2489,.T.);
#3346=EDGE_CURVE('',#2813,#2812,#1775,.T.);
#3347=EDGE_CURVE('',#2814,#2815,#1776,.T.);
#3348=EDGE_CURVE('',#2815,#2816,#1777,.T.);
#3349=EDGE_CURVE('',#2816,#2817,#1778,.T.);
#3350=EDGE_CURVE('',#2814,#2817,#1779,.T.);
#3351=EDGE_CURVE('',#2815,#2818,#1780,.T.);
#3352=EDGE_CURVE('',#2818,#2819,#1781,.T.);
#3353=EDGE_CURVE('',#2819,#2816,#1782,.T.);
#3354=EDGE_CURVE('',#2818,#2820,#1783,.T.);
#3355=EDGE_CURVE('',#2820,#2821,#1784,.T.);
#3356=EDGE_CURVE('',#2821,#2819,#1785,.T.);
#3357=EDGE_CURVE('',#2820,#2822,#1786,.T.);
#3358=EDGE_CURVE('',#2822,#2823,#1787,.T.);
#3359=EDGE_CURVE('',#2823,#2821,#1788,.T.);
#3360=EDGE_CURVE('',#2822,#2824,#1789,.T.);
#3361=EDGE_CURVE('',#2824,#2825,#1790,.T.);
#3362=EDGE_CURVE('',#2825,#2823,#1791,.T.);
#3363=EDGE_CURVE('',#2824,#2814,#1792,.T.);
#3364=EDGE_CURVE('',#2817,#2825,#1793,.T.);
#4270=ORIENTED_EDGE('',*,*,#3333,.F.);
#4271=ORIENTED_EDGE('',*,*,#3334,.F.);
#4272=ORIENTED_EDGE('',*,*,#3335,.T.);
#4273=ORIENTED_EDGE('',*,*,#3333,.T.);
#4274=ORIENTED_EDGE('',*,*,#3335,.F.);
#4275=ORIENTED_EDGE('',*,*,#3336,.F.);
#4276=ORIENTED_EDGE('',*,*,#3337,.T.);
#4277=ORIENTED_EDGE('',*,*,#3334,.T.);
#4278=ORIENTED_EDGE('',*,*,#3337,.F.);
#4279=ORIENTED_EDGE('',*,*,#3338,.F.);
#4280=ORIENTED_EDGE('',*,*,#3339,.T.);
#4281=ORIENTED_EDGE('',*,*,#3336,.T.);
#4282=ORIENTED_EDGE('',*,*,#3339,.F.);
#4283=ORIENTED_EDGE('',*,*,#3338,.T.);
#4284=ORIENTED_EDGE('',*,*,#3340,.F.);
#4285=ORIENTED_EDGE('',*,*,#3341,.F.);
#4286=ORIENTED_EDGE('',*,*,#3342,.T.);
#4287=ORIENTED_EDGE('',*,*,#3340,.T.);
#4288=ORIENTED_EDGE('',*,*,#3342,.F.);
#4289=ORIENTED_EDGE('',*,*,#3343,.F.);
#4290=ORIENTED_EDGE('',*,*,#3344,.T.);
#4291=ORIENTED_EDGE('',*,*,#3341,.T.);
#4292=ORIENTED_EDGE('',*,*,#3344,.F.);
#4293=ORIENTED_EDGE('',*,*,#3345,.F.);
#4294=ORIENTED_EDGE('',*,*,#3346,.T.);
#4295=ORIENTED_EDGE('',*,*,#3343,.T.);
#4296=ORIENTED_EDGE('',*,*,#3346,.F.);
#4297=ORIENTED_EDGE('',*,*,#3345,.T.);
#4298=ORIENTED_EDGE('',*,*,#3347,.T.);
#4299=ORIENTED_EDGE('',*,*,#3348,.T.);
#4300=ORIENTED_EDGE('',*,*,#3349,.T.);
#4301=ORIENTED_EDGE('',*,*,#3350,.F.);
#4302=ORIENTED_EDGE('',*,*,#3351,.T.);
#4303=ORIENTED_EDGE('',*,*,#3352,.T.);
#4304=ORIENTED_EDGE('',*,*,#3353,.T.);
#4305=ORIENTED_EDGE('',*,*,#3348,.F.);
#4306=ORIENTED_EDGE('',*,*,#3354,.T.);
#4307=ORIENTED_EDGE('',*,*,#3355,.T.);
#4308=ORIENTED_EDGE('',*,*,#3356,.T.);
#4309=ORIENTED_EDGE('',*,*,#3352,.F.);
#4310=ORIENTED_EDGE('',*,*,#3357,.T.);
#4311=ORIENTED_EDGE('',*,*,#3358,.T.);
#4312=ORIENTED_EDGE('',*,*,#3359,.T.);
#4313=ORIENTED_EDGE('',*,*,#3355,.F.);
#4314=ORIENTED_EDGE('',*,*,#3360,.T.);
#4315=ORIENTED_EDGE('',*,*,#3361,.T.);
#4316=ORIENTED_EDGE('',*,*,#3362,.T.);
#4317=ORIENTED_EDGE('',*,*,#3358,.F.);
#4318=ORIENTED_EDGE('',*,*,#3363,.T.);
#4319=ORIENTED_EDGE('',*,*,#3350,.T.);
#4320=ORIENTED_EDGE('',*,*,#3364,.T.);
#4321=ORIENTED_EDGE('',*,*,#3361,.F.);
#4322=ORIENTED_EDGE('',*,*,#3363,.F.);
#4323=ORIENTED_EDGE('',*,*,#3360,.F.);
#4324=ORIENTED_EDGE('',*,*,#3357,.F.);
#4325=ORIENTED_EDGE('',*,*,#3354,.F.);
#4326=ORIENTED_EDGE('',*,*,#3351,.F.);
#4327=ORIENTED_EDGE('',*,*,#3347,.F.);
#4328=ORIENTED_EDGE('',*,*,#3364,.F.);
#4329=ORIENTED_EDGE('',*,*,#3349,.F.);
#4330=ORIENTED_EDGE('',*,*,#3353,.F.);
#4331=ORIENTED_EDGE('',*,*,#3356,.F.);
#4332=ORIENTED_EDGE('',*,*,#3359,.F.);
#4333=ORIENTED_EDGE('',*,*,#3362,.F.);
#5126=CYLINDRICAL_SURFACE('',#6161,0.35);
#5127=CYLINDRICAL_SURFACE('',#6169,0.1954);
#5313=ADVANCED_FACE('',(#964),#708,.T.);
#5314=ADVANCED_FACE('',(#965),#357,.T.);
#5315=ADVANCED_FACE('',(#966),#5126,.T.);
#5316=ADVANCED_FACE('',(#967),#358,.T.);
#5317=ADVANCED_FACE('',(#968,#576),#709,.T.);
#5318=ADVANCED_FACE('',(#969),#359,.T.);
#5319=ADVANCED_FACE('',(#970),#5127,.T.);
#5320=ADVANCED_FACE('',(#971),#360,.T.);
#5321=ADVANCED_FACE('',(#972),#710,.T.);
#5322=ADVANCED_FACE('',(#973),#711,.F.);
#5323=ADVANCED_FACE('',(#974),#712,.F.);
#5324=ADVANCED_FACE('',(#975),#713,.F.);
#5325=ADVANCED_FACE('',(#976),#714,.F.);
#5326=ADVANCED_FACE('',(#977),#715,.F.);
#5327=ADVANCED_FACE('',(#978),#716,.F.);
#5328=ADVANCED_FACE('',(#979),#717,.F.);
#5329=ADVANCED_FACE('',(#980),#718,.F.);
#5529=CLOSED_SHELL('',(#5313,#5314,#5315,#5316,#5317,#5318,#5319,#5320,
#5321));
#5530=CLOSED_SHELL('',(#5322,#5323,#5324,#5325,#5326,#5327,#5328,#5329));
#6156=AXIS2_PLACEMENT_3D('',#9033,#7268,#7269);
#6157=AXIS2_PLACEMENT_3D('',#9034,#7270,#7271);
#6158=AXIS2_PLACEMENT_3D('',#9036,#7272,#7273);
#6159=AXIS2_PLACEMENT_3D('',#9037,#7274,#7275);
#6160=AXIS2_PLACEMENT_3D('',#9039,#7276,#7277);
#6161=AXIS2_PLACEMENT_3D('',#9041,#7279,#7280);
#6162=AXIS2_PLACEMENT_3D('',#9043,#7281,#7282);
#6163=AXIS2_PLACEMENT_3D('',#9045,#7284,#7285);
#6164=AXIS2_PLACEMENT_3D('',#9047,#7286,#7287);
#6165=AXIS2_PLACEMENT_3D('',#9049,#7289,#7290);
#6166=AXIS2_PLACEMENT_3D('',#9051,#7291,#7292);
#6167=AXIS2_PLACEMENT_3D('',#9052,#7293,#7294);
#6168=AXIS2_PLACEMENT_3D('',#9054,#7295,#7296);
#6169=AXIS2_PLACEMENT_3D('',#9056,#7298,#7299);
#6170=AXIS2_PLACEMENT_3D('',#9058,#7300,#7301);
#6171=AXIS2_PLACEMENT_3D('',#9060,#7303,#7304);
#6172=AXIS2_PLACEMENT_3D('',#9062,#7305,#7306);
#6173=AXIS2_PLACEMENT_3D('',#9064,#7308,#7309);
#6174=AXIS2_PLACEMENT_3D('',#9065,#7310,#7311);
#6175=AXIS2_PLACEMENT_3D('',#9074,#7316,#7317);
#6176=AXIS2_PLACEMENT_3D('',#9080,#7321,#7322);
#6177=AXIS2_PLACEMENT_3D('',#9086,#7326,#7327);
#6178=AXIS2_PLACEMENT_3D('',#9092,#7331,#7332);
#6179=AXIS2_PLACEMENT_3D('',#9098,#7336,#7337);
#6180=AXIS2_PLACEMENT_3D('',#9101,#7340,#7341);
#6181=AXIS2_PLACEMENT_3D('',#9102,#7342,#7343);
#7268=DIRECTION('axis',(0.,0.,1.));
#7269=DIRECTION('refdir',(1.,0.,0.));
#7270=DIRECTION('center_axis',(0.,1.,0.));
#7271=DIRECTION('ref_axis',(0.,0.,1.));
#7272=DIRECTION('center_axis',(0.,-1.,0.));
#7273=DIRECTION('ref_axis',(1.,0.,0.));
#7274=DIRECTION('center_axis',(0.,-1.,0.));
#7275=DIRECTION('ref_axis',(1.,0.,0.));
#7276=DIRECTION('center_axis',(0.,-1.,0.));
#7277=DIRECTION('ref_axis',(1.,0.,0.));
#7278=DIRECTION('',(0.707106781186547,0.707106781186548,8.65956056235493E-17));
#7279=DIRECTION('center_axis',(0.,-1.,0.));
#7280=DIRECTION('ref_axis',(1.,0.,0.));
#7281=DIRECTION('center_axis',(0.,-1.,0.));
#7282=DIRECTION('ref_axis',(1.,0.,0.));
#7283=DIRECTION('',(0.,1.,0.));
#7284=DIRECTION('center_axis',(0.,1.,0.));
#7285=DIRECTION('ref_axis',(1.,0.,0.));
#7286=DIRECTION('center_axis',(0.,-1.,0.));
#7287=DIRECTION('ref_axis',(1.,0.,0.));
#7288=DIRECTION('',(-0.707106781186547,0.707106781186548,-8.65956056235493E-17));
#7289=DIRECTION('center_axis',(0.,-1.,0.));
#7290=DIRECTION('ref_axis',(0.,0.,-1.));
#7291=DIRECTION('center_axis',(0.,-1.,0.));
#7292=DIRECTION('ref_axis',(1.,0.,0.));
#7293=DIRECTION('center_axis',(0.,1.,0.));
#7294=DIRECTION('ref_axis',(1.,0.,0.));
#7295=DIRECTION('center_axis',(0.,1.,0.));
#7296=DIRECTION('ref_axis',(1.,0.,0.));
#7297=DIRECTION('',(-0.447213595499958,0.894427190999916,-5.47678698264203E-17));
#7298=DIRECTION('center_axis',(0.,-1.,0.));
#7299=DIRECTION('ref_axis',(1.,0.,0.));
#7300=DIRECTION('center_axis',(0.,1.,0.));
#7301=DIRECTION('ref_axis',(1.,0.,0.));
#7302=DIRECTION('',(0.,1.,0.));
#7303=DIRECTION('center_axis',(0.,1.,0.));
#7304=DIRECTION('ref_axis',(1.,0.,0.));
#7305=DIRECTION('center_axis',(0.,-1.,0.));
#7306=DIRECTION('ref_axis',(1.,0.,0.));
#7307=DIRECTION('',(-0.707106781186547,0.707106781186548,-8.65956056235493E-17));
#7308=DIRECTION('center_axis',(0.,-1.,0.));
#7309=DIRECTION('ref_axis',(0.,0.,-1.));
#7310=DIRECTION('center_axis',(0.866025403784439,0.,-0.5));
#7311=DIRECTION('ref_axis',(0.5,0.,0.866025403784439));
#7312=DIRECTION('',(-0.5,0.,-0.866025403784439));
#7313=DIRECTION('',(0.,-1.,0.));
#7314=DIRECTION('',(0.5,0.,0.866025403784439));
#7315=DIRECTION('',(0.,-1.,0.));
#7316=DIRECTION('center_axis',(1.60246890531964E-16,0.,-1.));
#7317=DIRECTION('ref_axis',(1.,0.,1.60246890531964E-16));
#7318=DIRECTION('',(-1.,0.,-1.60246890531964E-16));
#7319=DIRECTION('',(0.,-1.,0.));
#7320=DIRECTION('',(1.,0.,1.60246890531964E-16));
#7321=DIRECTION('center_axis',(-0.866025403784439,0.,-0.5));
#7322=DIRECTION('ref_axis',(0.5,0.,-0.866025403784439));
#7323=DIRECTION('',(-0.5,0.,0.866025403784439));
#7324=DIRECTION('',(0.,-1.,0.));
#7325=DIRECTION('',(0.5,0.,-0.866025403784439));
#7326=DIRECTION('center_axis',(-0.866025403784439,0.,0.5));
#7327=DIRECTION('ref_axis',(-0.5,0.,-0.866025403784439));
#7328=DIRECTION('',(0.5,0.,0.866025403784439));
#7329=DIRECTION('',(0.,-1.,0.));
#7330=DIRECTION('',(-0.5,0.,-0.866025403784439));
#7331=DIRECTION('center_axis',(-1.60246890531964E-16,0.,1.));
#7332=DIRECTION('ref_axis',(-1.,0.,-1.60246890531964E-16));
#7333=DIRECTION('',(1.,0.,1.60246890531964E-16));
#7334=DIRECTION('',(0.,-1.,0.));
#7335=DIRECTION('',(-1.,0.,-1.60246890531964E-16));
#7336=DIRECTION('center_axis',(0.866025403784439,0.,0.5));
#7337=DIRECTION('ref_axis',(-0.5,0.,0.866025403784439));
#7338=DIRECTION('',(0.5,0.,-0.866025403784439));
#7339=DIRECTION('',(-0.5,0.,0.866025403784439));
#7340=DIRECTION('center_axis',(0.,1.,0.));
#7341=DIRECTION('ref_axis',(1.,0.,0.));
#7342=DIRECTION('center_axis',(0.,-1.,0.));
#7343=DIRECTION('ref_axis',(0.,0.,-1.));
#9033=CARTESIAN_POINT('',(0.,0.,0.));
#9034=CARTESIAN_POINT('Origin',(0.3,0.4,0.));
#9035=CARTESIAN_POINT('',(-0.3,0.4,-3.67394039744206E-17));
#9036=CARTESIAN_POINT('Origin',(0.,0.4,0.));
#9037=CARTESIAN_POINT('Origin',(0.,0.375,0.));
#9038=CARTESIAN_POINT('',(-0.35,0.35,-4.28626379701573E-17));
#9039=CARTESIAN_POINT('Origin',(0.,0.35,0.));
#9040=CARTESIAN_POINT('',(-0.325,0.375,-3.9801020972289E-17));
#9041=CARTESIAN_POINT('Origin',(0.,0.19,0.));
#9042=CARTESIAN_POINT('',(-0.35,0.03,-4.28626379701574E-17));
#9043=CARTESIAN_POINT('Origin',(0.,0.03,0.));
#9044=CARTESIAN_POINT('',(-0.35,0.19,-4.28626379701574E-17));
#9045=CARTESIAN_POINT('Origin',(0.,0.0149999999999999,0.));
#9046=CARTESIAN_POINT('',(-0.32,-3.29597460435593E-17,-3.91886975727153E-17));
#9047=CARTESIAN_POINT('Origin',(0.,0.,0.));
#9048=CARTESIAN_POINT('',(-0.335,0.0149999999999999,-4.10256677714363E-17));
#9049=CARTESIAN_POINT('Origin',(0.22,0.,0.));
#9050=CARTESIAN_POINT('',(-0.22,-6.93889390390723E-18,-2.69422295812418E-17));
#9051=CARTESIAN_POINT('Origin',(0.,0.,0.));
#9052=CARTESIAN_POINT('Origin',(0.,-0.02,0.));
#9053=CARTESIAN_POINT('',(-0.1954,-0.0492,2.39295984553393E-17));
#9054=CARTESIAN_POINT('Origin',(0.,-0.0492,0.));
#9055=CARTESIAN_POINT('',(-0.21,-0.02,-2.57175827820944E-17));
#9056=CARTESIAN_POINT('Origin',(0.,-0.8,0.));
#9057=CARTESIAN_POINT('',(-0.1954,-1.5646,2.39295984553393E-17));
#9058=CARTESIAN_POINT('Origin',(0.,-1.5646,0.));
#9059=CARTESIAN_POINT('',(-0.1954,-0.8,-2.39295984553393E-17));
#9060=CARTESIAN_POINT('Origin',(0.,-1.58,0.));
#9061=CARTESIAN_POINT('',(-0.16,-1.6,-1.95943487863577E-17));
#9062=CARTESIAN_POINT('Origin',(0.,-1.6,0.));
#9063=CARTESIAN_POINT('',(-0.18,-1.58,-2.20436423846524E-17));
#9064=CARTESIAN_POINT('Origin',(0.,-1.6,0.));
#9065=CARTESIAN_POINT('Origin',(0.0866025403784439,-0.4,-0.15));
#9066=CARTESIAN_POINT('',(0.173205080756888,-0.4,0.));
#9067=CARTESIAN_POINT('',(0.0866025403784439,-0.4,-0.15));
#9068=CARTESIAN_POINT('',(0.173205080756888,-0.4,0.));
#9069=CARTESIAN_POINT('',(0.0866025403784439,-0.64,-0.15));
#9070=CARTESIAN_POINT('',(0.0866025403784439,-0.4,-0.15));
#9071=CARTESIAN_POINT('',(0.173205080756888,-0.64,0.));
#9072=CARTESIAN_POINT('',(0.173205080756888,-0.64,0.));
#9073=CARTESIAN_POINT('',(0.173205080756888,-0.4,0.));
#9074=CARTESIAN_POINT('Origin',(-0.0866025403784438,-0.4,-0.15));
#9075=CARTESIAN_POINT('',(-0.0866025403784438,-0.4,-0.15));
#9076=CARTESIAN_POINT('',(0.0866025403784439,-0.4,-0.15));
#9077=CARTESIAN_POINT('',(-0.0866025403784438,-0.64,-0.15));
#9078=CARTESIAN_POINT('',(-0.0866025403784438,-0.4,-0.15));
#9079=CARTESIAN_POINT('',(0.0866025403784439,-0.64,-0.15));
#9080=CARTESIAN_POINT('Origin',(-0.173205080756888,-0.4,-2.77555756156289E-17));
#9081=CARTESIAN_POINT('',(-0.173205080756888,-0.4,-2.12115047744981E-17));
#9082=CARTESIAN_POINT('',(-0.0866025403784438,-0.4,-0.15));
#9083=CARTESIAN_POINT('',(-0.173205080756888,-0.64,-2.77555756156289E-17));
#9084=CARTESIAN_POINT('',(-0.173205080756888,-0.4,-2.12115047744981E-17));
#9085=CARTESIAN_POINT('',(-0.0866025403784438,-0.64,-0.15));
#9086=CARTESIAN_POINT('Origin',(-0.0866025403784439,-0.4,0.15));
#9087=CARTESIAN_POINT('',(-0.0866025403784439,-0.4,0.15));
#9088=CARTESIAN_POINT('',(-0.173205080756888,-0.4,-2.12115047744981E-17));
#9089=CARTESIAN_POINT('',(-0.0866025403784439,-0.64,0.15));
#9090=CARTESIAN_POINT('',(-0.0866025403784439,-0.4,0.15));
#9091=CARTESIAN_POINT('',(-0.173205080756888,-0.64,-2.12115047744981E-17));
#9092=CARTESIAN_POINT('Origin',(0.0866025403784439,-0.4,0.15));
#9093=CARTESIAN_POINT('',(0.0866025403784439,-0.4,0.15));
#9094=CARTESIAN_POINT('',(-0.0866025403784439,-0.4,0.15));
#9095=CARTESIAN_POINT('',(0.0866025403784439,-0.64,0.15));
#9096=CARTESIAN_POINT('',(0.0866025403784439,-0.4,0.15));
#9097=CARTESIAN_POINT('',(-0.0866025403784439,-0.64,0.15));
#9098=CARTESIAN_POINT('Origin',(0.173205080756888,-0.4,0.));
#9099=CARTESIAN_POINT('',(0.0866025403784439,-0.4,0.15));
#9100=CARTESIAN_POINT('',(0.0866025403784439,-0.64,0.15));
#9101=CARTESIAN_POINT('Origin',(0.,-0.4,-2.77555756156289E-17));
#9102=CARTESIAN_POINT('Origin',(0.,-0.64,-2.77555756156289E-17));
#10037=UNCERTAINTY_MEASURE_WITH_UNIT(LENGTH_MEASURE(0.001),#10096,
'DISTANCE_ACCURACY_VALUE',
'Maximum model space distance between geometric entities at asserted c
onnectivities');
#10058=UNCERTAINTY_MEASURE_WITH_UNIT(LENGTH_MEASURE(0.001),#10096,
'DISTANCE_ACCURACY_VALUE',
'Maximum model space distance between geometric entities at asserted c
onnectivities');
#10074=(
GEOMETRIC_REPRESENTATION_CONTEXT(3)
GLOBAL_UNCERTAINTY_ASSIGNED_CONTEXT((#10037))
GLOBAL_UNIT_ASSIGNED_CONTEXT((#10096,#10098,#10099))
REPRESENTATION_CONTEXT('','3D')
);
#10095=(
GEOMETRIC_REPRESENTATION_CONTEXT(3)
GLOBAL_UNCERTAINTY_ASSIGNED_CONTEXT((#10058))
GLOBAL_UNIT_ASSIGNED_CONTEXT((#10096,#10098,#10099))
REPRESENTATION_CONTEXT('','3D')
);
#10096=(
LENGTH_UNIT()
NAMED_UNIT(*)
SI_UNIT(.CENTI.,.METRE.)
);
#10098=(
NAMED_UNIT(*)
PLANE_ANGLE_UNIT()
SI_UNIT($,.RADIAN.)
);
#10099=(
NAMED_UNIT(*)
SI_UNIT($,.STERADIAN.)
SOLID_ANGLE_UNIT()
);
#10115=SHAPE_DEFINITION_REPRESENTATION(#10151,#10262);
#10151=PRODUCT_DEFINITION_SHAPE('',$,#10299);
#10262=SHAPE_REPRESENTATION('',(#6156),#10074);
#10283=PRODUCT_DEFINITION_CONTEXT('part definition',#10393,'design');
#10299=PRODUCT_DEFINITION('Cap Screw - M4x16','Cap Screw - M4x16',#10335,
#10283);
#10335=PRODUCT_DEFINITION_FORMATION('',$,#10410);
#10393=APPLICATION_CONTEXT(
'Core Data for Automotive Mechanical Design Process');
#10394=PRODUCT_CONTEXT('part definition',#10393,'mechanical');
#10410=PRODUCT('Cap Screw - M4x16','Cap Screw - M4x16',
'Cap Screw - M4x16',(#10394));
#10501=COLOUR_RGB('Black',0.12,0.14,0.17);
#10502=FILL_AREA_STYLE_COLOUR('',#10501);
#10503=FILL_AREA_STYLE('',(#10502));
#10504=SURFACE_STYLE_FILL_AREA(#10503);
#10505=SURFACE_SIDE_STYLE('',(#10504));
#10506=SURFACE_STYLE_USAGE(.BOTH.,#10505);
#10507=PRESENTATION_STYLE_ASSIGNMENT((#10506));
ENDSEC;
END-ISO-10303-21;
